ISO-10303-21;
HEADER;
/* Generated by software containing ST-Developer
 * from STEP Tools, Inc. (www.steptools.com) 
 */

FILE_DESCRIPTION(
/* description */ ('Four-bar parallelogram arm'),
/* implementation_level */ '2;1');

FILE_NAME(
/* name */ 'Outer race spacer (2).step',
/* time_stamp */ '2026-10-28T03:24:55-07:00',
/* author */ (''),
/* organization */ (''),
/* preprocessor_version */ 'ST-DEVELOPER v20.2',
/* originating_system */ 'Autodesk Translation Framework v15.17.0.0',
/* authorisation */ '');

FILE_SCHEMA (('AUTOMOTIVE_DESIGN { 1 0 10303 214 3 1 1 }'));
ENDSEC;

DATA;
#10=MECHANICAL_DESIGN_GEOMETRIC_PRESENTATION_REPRESENTATION('',(#648),#14512);
#548=SHAPE_REPRESENTATION_RELATIONSHIP('SRR','None',#14771,#598);
#598=ADVANCED_BREP_SHAPE_REPRESENTATION('',(#705),#14486);
#648=STYLED_ITEM('',(#15087),#705);
#705=MANIFOLD_SOLID_BREP('Body1',#7353);
#893=FACE_BOUND('',#2001,.T.);
#894=FACE_BOUND('',#2003,.T.);
#1115=PLANE('',#8411);
#1116=PLANE('',#8412);
#1420=FACE_OUTER_BOUND('',#1998,.T.);
#1421=FACE_OUTER_BOUND('',#1999,.T.);
#1422=FACE_OUTER_BOUND('',#2000,.T.);
#1423=FACE_OUTER_BOUND('',#2002,.T.);
#1998=EDGE_LOOP('',(#5916,#5917,#5918,#5919));
#1999=EDGE_LOOP('',(#5920,#5921,#5922,#5923));
#2000=EDGE_LOOP('',(#5924));
#2001=EDGE_LOOP('',(#5925));
#2002=EDGE_LOOP('',(#5926));
#2003=EDGE_LOOP('',(#5927));
#2552=LINE('',#13055,#2946);
#2553=LINE('',#13061,#2947);
#2946=VECTOR('',#10148,1.02);
#2947=VECTOR('',#10155,1.49);
#3318=CIRCLE('',#8406,1.02);
#3319=CIRCLE('',#8407,1.02);
#3320=CIRCLE('',#8409,1.49);
#3321=CIRCLE('',#8410,1.49);
#3852=VERTEX_POINT('',#13052);
#3853=VERTEX_POINT('',#13054);
#3854=VERTEX_POINT('',#13058);
#3855=VERTEX_POINT('',#13060);
#4589=EDGE_CURVE('',#3852,#3852,#3318,.T.);
#4590=EDGE_CURVE('',#3852,#3853,#2552,.T.);
#4591=EDGE_CURVE('',#3853,#3853,#3319,.T.);
#4592=EDGE_CURVE('',#3854,#3854,#3320,.T.);
#4593=EDGE_CURVE('',#3854,#3855,#2553,.T.);
#4594=EDGE_CURVE('',#3855,#3855,#3321,.T.);
#5916=ORIENTED_EDGE('',*,*,#4589,.F.);
#5917=ORIENTED_EDGE('',*,*,#4590,.T.);
#5918=ORIENTED_EDGE('',*,*,#4591,.T.);
#5919=ORIENTED_EDGE('',*,*,#4590,.F.);
#5920=ORIENTED_EDGE('',*,*,#4592,.F.);
#5921=ORIENTED_EDGE('',*,*,#4593,.T.);
#5922=ORIENTED_EDGE('',*,*,#4594,.T.);
#5923=ORIENTED_EDGE('',*,*,#4593,.F.);
#5924=ORIENTED_EDGE('',*,*,#4592,.T.);
#5925=ORIENTED_EDGE('',*,*,#4589,.T.);
#5926=ORIENTED_EDGE('',*,*,#4594,.F.);
#5927=ORIENTED_EDGE('',*,*,#4591,.F.);
#6820=CYLINDRICAL_SURFACE('',#8405,1.02);
#6821=CYLINDRICAL_SURFACE('',#8408,1.49);
#7125=ADVANCED_FACE('',(#1420),#6820,.F.);
#7126=ADVANCED_FACE('',(#1421),#6821,.T.);
#7127=ADVANCED_FACE('',(#1422,#893),#1115,.T.);
#7128=ADVANCED_FACE('',(#1423,#894),#1116,.F.);
#7353=CLOSED_SHELL('',(#7125,#7126,#7127,#7128));
#8404=AXIS2_PLACEMENT_3D('',#13050,#10142,#10143);
#8405=AXIS2_PLACEMENT_3D('',#13051,#10144,#10145);
#8406=AXIS2_PLACEMENT_3D('',#13053,#10146,#10147);
#8407=AXIS2_PLACEMENT_3D('',#13056,#10149,#10150);
#8408=AXIS2_PLACEMENT_3D('',#13057,#10151,#10152);
#8409=AXIS2_PLACEMENT_3D('',#13059,#10153,#10154);
#8410=AXIS2_PLACEMENT_3D('',#13062,#10156,#10157);
#8411=AXIS2_PLACEMENT_3D('',#13063,#10158,#10159);
#8412=AXIS2_PLACEMENT_3D('',#13064,#10160,#10161);
#10142=DIRECTION('axis',(0.,0.,1.));
#10143=DIRECTION('refdir',(1.,0.,0.));
#10144=DIRECTION('center_axis',(0.,1.,0.));
#10145=DIRECTION('ref_axis',(1.,0.,0.));
#10146=DIRECTION('center_axis',(0.,-1.,0.));
#10147=DIRECTION('ref_axis',(1.,0.,0.));
#10148=DIRECTION('',(0.,-1.,0.));
#10149=DIRECTION('center_axis',(0.,-1.,0.));
#10150=DIRECTION('ref_axis',(1.,0.,0.));
#10151=DIRECTION('center_axis',(0.,1.,0.));
#10152=DIRECTION('ref_axis',(1.,0.,0.));
#10153=DIRECTION('center_axis',(0.,1.,0.));
#10154=DIRECTION('ref_axis',(1.,0.,0.));
#10155=DIRECTION('',(0.,-1.,0.));
#10156=DIRECTION('center_axis',(0.,1.,0.));
#10157=DIRECTION('ref_axis',(1.,0.,0.));
#10158=DIRECTION('center_axis',(0.,1.,0.));
#10159=DIRECTION('ref_axis',(1.,0.,0.));
#10160=DIRECTION('center_axis',(0.,1.,0.));
#10161=DIRECTION('ref_axis',(1.,0.,0.));
#13050=CARTESIAN_POINT('',(0.,0.,0.));
#13051=CARTESIAN_POINT('Origin',(0.,-0.15,14.));
#13052=CARTESIAN_POINT('',(-1.02,0.15,14.));
#13053=CARTESIAN_POINT('Origin',(0.,0.15,14.));
#13054=CARTESIAN_POINT('',(-1.02,-0.15,14.));
#13055=CARTESIAN_POINT('',(-1.02,-0.15,14.));
#13056=CARTESIAN_POINT('Origin',(0.,-0.15,14.));
#13057=CARTESIAN_POINT('Origin',(0.,-0.15,14.));
#13058=CARTESIAN_POINT('',(-1.49,0.15,14.));
#13059=CARTESIAN_POINT('Origin',(0.,0.15,14.));
#13060=CARTESIAN_POINT('',(-1.49,-0.15,14.));
#13061=CARTESIAN_POINT('',(-1.49,-0.15,14.));
#13062=CARTESIAN_POINT('Origin',(0.,-0.15,14.));
#13063=CARTESIAN_POINT('Origin',(0.,0.15,14.));
#13064=CARTESIAN_POINT('Origin',(0.,-0.15,14.));
#14429=UNCERTAINTY_MEASURE_WITH_UNIT(LENGTH_MEASURE(0.001),#14513,
'DISTANCE_ACCURACY_VALUE',
'Maximum model space distance between geometric entities at asserted c
onnectivities');
#14455=UNCERTAINTY_MEASURE_WITH_UNIT(LENGTH_MEASURE(0.001),#14513,
'DISTANCE_ACCURACY_VALUE',
'Maximum model space distance between geometric entities at asserted c
onnectivities');
#14486=(
GEOMETRIC_REPRESENTATION_CONTEXT(3)
GLOBAL_UNCERTAINTY_ASSIGNED_CONTEXT((#14429))
GLOBAL_UNIT_ASSIGNED_CONTEXT((#14513,#14515,#14516))
REPRESENTATION_CONTEXT('','3D')
);
#14512=(
GEOMETRIC_REPRESENTATION_CONTEXT(3)
GLOBAL_UNCERTAINTY_ASSIGNED_CONTEXT((#14455))
GLOBAL_UNIT_ASSIGNED_CONTEXT((#14513,#14515,#14516))
REPRESENTATION_CONTEXT('','3D')
);
#14513=(
LENGTH_UNIT()
NAMED_UNIT(*)
SI_UNIT(.CENTI.,.METRE.)
);
#14515=(
NAMED_UNIT(*)
PLANE_ANGLE_UNIT()
SI_UNIT($,.RADIAN.)
);
#14516=(
NAMED_UNIT(*)
SI_UNIT($,.STERADIAN.)
SOLID_ANGLE_UNIT()
);
#14547=SHAPE_DEFINITION_REPRESENTATION(#14603,#14771);
#14603=PRODUCT_DEFINITION_SHAPE('',$,#14828);
#14771=SHAPE_REPRESENTATION('',(#8404),#14486);
#14797=PRODUCT_DEFINITION_CONTEXT('part definition',#14967,'design');
#14828=PRODUCT_DEFINITION('Outer race spacer (2)','Outer race spacer (2)',
#14884,#14797);
#14884=PRODUCT_DEFINITION_FORMATION('',$,#14999);
#14967=APPLICATION_CONTEXT(
'Core Data for Automotive Mechanical Design Process');
#14968=PRODUCT_CONTEXT('part definition',#14967,'mechanical');
#14999=PRODUCT('Outer race spacer (2)','Outer race spacer (2)',
'Outer race spacer (2)',(#14968));
#15081=COLOUR_RGB('Grey',0.48,0.52,0.57);
#15082=FILL_AREA_STYLE_COLOUR('',#15081);
#15083=FILL_AREA_STYLE('',(#15082));
#15084=SURFACE_STYLE_FILL_AREA(#15083);
#15085=SURFACE_SIDE_STYLE('',(#15084));
#15086=SURFACE_STYLE_USAGE(.BOTH.,#15085);
#15087=PRESENTATION_STYLE_ASSIGNMENT((#15086));
ENDSEC;
END-ISO-10303-21;
